ISO-10303-21;
HEADER;
/* Generated by software containing ST-Developer
 * from STEP Tools, Inc. (www.steptools.com) 
 */

FILE_DESCRIPTION(
/* description */ ('Independent four-jaw lathe chuck,200mm body,40mm bore,36\X2\2013\X0\7
6mm nominal opposed jaw opening. Four shared machined T-jaws and model
ed partial M12x1.75 feed screws, native independent screw/slider links
, removable bolted bronze-bearing cartridges, fully captured ring/wash
er/head thrust stacks and registered bolted backplate. Custom spindle 
interface; no compatibility, speed, grip force or safety rating assign
ed.'),
/* implementation_level */ '2;1');

FILE_NAME(
/* name */ 'Screw retaining ring.step',
/* time_stamp */ '2026-11-09T20:24:54-08:00',
/* author */ (''),
/* organization */ (''),
/* preprocessor_version */ 'ST-DEVELOPER v20.2',
/* originating_system */ 'Autodesk Translation Framework v15.17.0.0',
/* authorisation */ '');

FILE_SCHEMA (('AUTOMOTIVE_DESIGN { 1 0 10303 214 3 1 1 }'));
ENDSEC;

DATA;
#10=MECHANICAL_DESIGN_GEOMETRIC_PRESENTATION_REPRESENTATION('',(#241),#69491);
#219=SHAPE_REPRESENTATION_RELATIONSHIP('SRR','None',#69576,#230);
#230=ADVANCED_BREP_SHAPE_REPRESENTATION('',(#252),#69485);
#241=STYLED_ITEM('',(#69640),#252);
#252=MANIFOLD_SOLID_BREP('Body1',#14736);
#492=PLANE('',#15587);
#493=PLANE('',#15588);
#494=PLANE('',#15589);
#495=PLANE('',#15596);
#1110=FACE_OUTER_BOUND('',#1948,.T.);
#1111=FACE_OUTER_BOUND('',#1949,.T.);
#1112=FACE_OUTER_BOUND('',#1950,.T.);
#1113=FACE_OUTER_BOUND('',#1951,.T.);
#1114=FACE_OUTER_BOUND('',#1952,.T.);
#1115=FACE_OUTER_BOUND('',#1953,.T.);
#1948=EDGE_LOOP('',(#12311,#12312,#12313,#12314));
#1949=EDGE_LOOP('',(#12315,#12316,#12317,#12318));
#1950=EDGE_LOOP('',(#12319,#12320,#12321,#12322));
#1951=EDGE_LOOP('',(#12323,#12324,#12325,#12326));
#1952=EDGE_LOOP('',(#12327,#12328,#12329,#12330));
#1953=EDGE_LOOP('',(#12331,#12332,#12333,#12334));
#2315=CIRCLE('',#15590,9.);
#2316=CIRCLE('',#15591,5.);
#2317=CIRCLE('',#15593,5.);
#2318=CIRCLE('',#15595,9.);
#4178=LINE('',#59239,#5026);
#4179=LINE('',#59241,#5027);
#4180=LINE('',#59243,#5028);
#4181=LINE('',#59244,#5029);
#4182=LINE('',#59248,#5030);
#4183=LINE('',#59250,#5031);
#4184=LINE('',#59252,#5032);
#4185=LINE('',#59253,#5033);
#5026=VECTOR('',#17962,10.);
#5027=VECTOR('',#17963,10.);
#5028=VECTOR('',#17964,10.);
#5029=VECTOR('',#17965,10.);
#5030=VECTOR('',#17968,10.);
#5031=VECTOR('',#17969,10.);
#5032=VECTOR('',#17970,10.);
#5033=VECTOR('',#17971,10.);
#6345=VERTEX_POINT('',#59237);
#6346=VERTEX_POINT('',#59238);
#6347=VERTEX_POINT('',#59240);
#6348=VERTEX_POINT('',#59242);
#6349=VERTEX_POINT('',#59246);
#6350=VERTEX_POINT('',#59247);
#6351=VERTEX_POINT('',#59249);
#6352=VERTEX_POINT('',#59251);
#8392=EDGE_CURVE('',#6345,#6346,#4178,.T.);
#8393=EDGE_CURVE('',#6347,#6345,#4179,.T.);
#8394=EDGE_CURVE('',#6348,#6347,#4180,.T.);
#8395=EDGE_CURVE('',#6346,#6348,#4181,.T.);
#8396=EDGE_CURVE('',#6349,#6350,#4182,.T.);
#8397=EDGE_CURVE('',#6351,#6349,#4183,.T.);
#8398=EDGE_CURVE('',#6352,#6351,#4184,.T.);
#8399=EDGE_CURVE('',#6350,#6352,#4185,.T.);
#8400=EDGE_CURVE('',#6347,#6352,#2315,.T.);
#8401=EDGE_CURVE('',#6350,#6345,#2316,.T.);
#8402=EDGE_CURVE('',#6349,#6346,#2317,.T.);
#8403=EDGE_CURVE('',#6348,#6351,#2318,.T.);
#12311=ORIENTED_EDGE('',*,*,#8392,.F.);
#12312=ORIENTED_EDGE('',*,*,#8393,.F.);
#12313=ORIENTED_EDGE('',*,*,#8394,.F.);
#12314=ORIENTED_EDGE('',*,*,#8395,.F.);
#12315=ORIENTED_EDGE('',*,*,#8396,.F.);
#12316=ORIENTED_EDGE('',*,*,#8397,.F.);
#12317=ORIENTED_EDGE('',*,*,#8398,.F.);
#12318=ORIENTED_EDGE('',*,*,#8399,.F.);
#12319=ORIENTED_EDGE('',*,*,#8399,.T.);
#12320=ORIENTED_EDGE('',*,*,#8400,.F.);
#12321=ORIENTED_EDGE('',*,*,#8393,.T.);
#12322=ORIENTED_EDGE('',*,*,#8401,.F.);
#12323=ORIENTED_EDGE('',*,*,#8396,.T.);
#12324=ORIENTED_EDGE('',*,*,#8401,.T.);
#12325=ORIENTED_EDGE('',*,*,#8392,.T.);
#12326=ORIENTED_EDGE('',*,*,#8402,.F.);
#12327=ORIENTED_EDGE('',*,*,#8398,.T.);
#12328=ORIENTED_EDGE('',*,*,#8403,.F.);
#12329=ORIENTED_EDGE('',*,*,#8394,.T.);
#12330=ORIENTED_EDGE('',*,*,#8400,.T.);
#12331=ORIENTED_EDGE('',*,*,#8397,.T.);
#12332=ORIENTED_EDGE('',*,*,#8402,.T.);
#12333=ORIENTED_EDGE('',*,*,#8395,.T.);
#12334=ORIENTED_EDGE('',*,*,#8403,.T.);
#13794=CYLINDRICAL_SURFACE('',#15592,5.);
#13795=CYLINDRICAL_SURFACE('',#15594,9.);
#14538=ADVANCED_FACE('',(#1110),#492,.F.);
#14539=ADVANCED_FACE('',(#1111),#493,.F.);
#14540=ADVANCED_FACE('',(#1112),#494,.F.);
#14541=ADVANCED_FACE('',(#1113),#13794,.F.);
#14542=ADVANCED_FACE('',(#1114),#13795,.T.);
#14543=ADVANCED_FACE('',(#1115),#495,.T.);
#14736=CLOSED_SHELL('',(#14538,#14539,#14540,#14541,#14542,#14543));
#15586=AXIS2_PLACEMENT_3D('',#59235,#17958,#17959);
#15587=AXIS2_PLACEMENT_3D('',#59236,#17960,#17961);
#15588=AXIS2_PLACEMENT_3D('',#59245,#17966,#17967);
#15589=AXIS2_PLACEMENT_3D('',#59254,#17972,#17973);
#15590=AXIS2_PLACEMENT_3D('',#59255,#17974,#17975);
#15591=AXIS2_PLACEMENT_3D('',#59256,#17976,#17977);
#15592=AXIS2_PLACEMENT_3D('',#59257,#17978,#17979);
#15593=AXIS2_PLACEMENT_3D('',#59258,#17980,#17981);
#15594=AXIS2_PLACEMENT_3D('',#59259,#17982,#17983);
#15595=AXIS2_PLACEMENT_3D('',#59260,#17984,#17985);
#15596=AXIS2_PLACEMENT_3D('',#59261,#17986,#17987);
#17958=DIRECTION('axis',(0.,0.,1.));
#17959=DIRECTION('refdir',(1.,0.,0.));
#17960=DIRECTION('center_axis',(-1.,0.,0.));
#17961=DIRECTION('ref_axis',(0.,1.,0.));
#17962=DIRECTION('',(0.,0.,1.));
#17963=DIRECTION('',(0.,-1.,0.));
#17964=DIRECTION('',(0.,0.,-1.));
#17965=DIRECTION('',(0.,1.,0.));
#17966=DIRECTION('center_axis',(1.,0.,0.));
#17967=DIRECTION('ref_axis',(0.,-1.,0.));
#17968=DIRECTION('',(0.,0.,-1.));
#17969=DIRECTION('',(0.,-1.,0.));
#17970=DIRECTION('',(0.,0.,1.));
#17971=DIRECTION('',(0.,1.,0.));
#17972=DIRECTION('center_axis',(0.,0.,1.));
#17973=DIRECTION('ref_axis',(1.,0.,0.));
#17974=DIRECTION('center_axis',(0.,0.,1.));
#17975=DIRECTION('ref_axis',(1.,0.,0.));
#17976=DIRECTION('center_axis',(0.,0.,-1.));
#17977=DIRECTION('ref_axis',(1.,0.,0.));
#17978=DIRECTION('center_axis',(0.,0.,1.));
#17979=DIRECTION('ref_axis',(6.12323399573677E-17,-1.,0.));
#17980=DIRECTION('center_axis',(0.,0.,-1.));
#17981=DIRECTION('ref_axis',(1.,0.,0.));
#17982=DIRECTION('center_axis',(0.,0.,1.));
#17983=DIRECTION('ref_axis',(6.12323399573677E-17,-1.,0.));
#17984=DIRECTION('center_axis',(0.,0.,1.));
#17985=DIRECTION('ref_axis',(1.,0.,0.));
#17986=DIRECTION('center_axis',(0.,0.,1.));
#17987=DIRECTION('ref_axis',(1.,0.,0.));
#59235=CARTESIAN_POINT('',(0.,0.,0.));
#59236=CARTESIAN_POINT('Origin',(-1.,0.,1.));
#59237=CARTESIAN_POINT('',(-1.,4.89897948556636,0.));
#59238=CARTESIAN_POINT('',(-1.,4.89897948556636,1.));
#59239=CARTESIAN_POINT('',(-1.,4.89897948556636,0.));
#59240=CARTESIAN_POINT('',(-1.,8.94427190999916,0.));
#59241=CARTESIAN_POINT('',(-1.,0.,0.));
#59242=CARTESIAN_POINT('',(-1.,8.94427190999916,1.));
#59243=CARTESIAN_POINT('',(-1.,8.94427190999916,0.));
#59244=CARTESIAN_POINT('',(-1.,0.,1.));
#59245=CARTESIAN_POINT('Origin',(1.,18.,1.));
#59246=CARTESIAN_POINT('',(1.,4.89897948556636,1.));
#59247=CARTESIAN_POINT('',(1.,4.89897948556636,0.));
#59248=CARTESIAN_POINT('',(1.,4.89897948556636,0.));
#59249=CARTESIAN_POINT('',(1.,8.94427190999916,1.));
#59250=CARTESIAN_POINT('',(1.,9.,1.));
#59251=CARTESIAN_POINT('',(1.,8.94427190999916,0.));
#59252=CARTESIAN_POINT('',(1.,8.94427190999916,0.));
#59253=CARTESIAN_POINT('',(1.,9.,0.));
#59254=CARTESIAN_POINT('Origin',(0.,0.,0.));
#59255=CARTESIAN_POINT('Origin',(0.,0.,0.));
#59256=CARTESIAN_POINT('Origin',(0.,0.,0.));
#59257=CARTESIAN_POINT('Origin',(0.,0.,0.));
#59258=CARTESIAN_POINT('Origin',(0.,0.,1.));
#59259=CARTESIAN_POINT('Origin',(0.,0.,0.));
#59260=CARTESIAN_POINT('Origin',(0.,0.,1.));
#59261=CARTESIAN_POINT('Origin',(0.,0.,1.));
#69472=UNCERTAINTY_MEASURE_WITH_UNIT(LENGTH_MEASURE(0.01),#69492,
'DISTANCE_ACCURACY_VALUE',
'Maximum model space distance between geometric entities at asserted c
onnectivities');
#69478=UNCERTAINTY_MEASURE_WITH_UNIT(LENGTH_MEASURE(0.01),#69492,
'DISTANCE_ACCURACY_VALUE',
'Maximum model space distance between geometric entities at asserted c
onnectivities');
#69485=(
GEOMETRIC_REPRESENTATION_CONTEXT(3)
GLOBAL_UNCERTAINTY_ASSIGNED_CONTEXT((#69472))
GLOBAL_UNIT_ASSIGNED_CONTEXT((#69492,#69494,#69495))
REPRESENTATION_CONTEXT('','3D')
);
#69491=(
GEOMETRIC_REPRESENTATION_CONTEXT(3)
GLOBAL_UNCERTAINTY_ASSIGNED_CONTEXT((#69478))
GLOBAL_UNIT_ASSIGNED_CONTEXT((#69492,#69494,#69495))
REPRESENTATION_CONTEXT('','3D')
);
#69492=(
LENGTH_UNIT()
NAMED_UNIT(*)
SI_UNIT(.MILLI.,.METRE.)
);
#69494=(
NAMED_UNIT(*)
PLANE_ANGLE_UNIT()
SI_UNIT($,.RADIAN.)
);
#69495=(
NAMED_UNIT(*)
SI_UNIT($,.STERADIAN.)
SOLID_ANGLE_UNIT()
);
#69502=SHAPE_DEFINITION_REPRESENTATION(#69514,#69576);
#69514=PRODUCT_DEFINITION_SHAPE('',$,#69589);
#69576=SHAPE_REPRESENTATION('',(#15586),#69485);
#69582=PRODUCT_DEFINITION_CONTEXT('part definition',#69620,'design');
#69589=PRODUCT_DEFINITION('Screw retaining ring','Screw retaining ring',
#69601,#69582);
#69601=PRODUCT_DEFINITION_FORMATION('',$,#69628);
#69620=APPLICATION_CONTEXT(
'Core Data for Automotive Mechanical Design Process');
#69621=PRODUCT_CONTEXT('part definition',#69620,'mechanical');
#69628=PRODUCT('Screw retaining ring','Screw retaining ring',$,(#69621));
#69640=PRESENTATION_STYLE_ASSIGNMENT((#69650));
#69650=SURFACE_STYLE_USAGE(.BOTH.,#69660);
#69660=SURFACE_SIDE_STYLE('',(#69670));
#69670=SURFACE_STYLE_FILL_AREA(#69680);
#69680=FILL_AREA_STYLE('Dark gray',(#69690));
#69690=FILL_AREA_STYLE_COLOUR('Dark gray',#69700);
#69700=COLOUR_RGB('Dark gray',0.250980392156863,0.282352941176471,0.32156862745098);
ENDSEC;
END-ISO-10303-21;
